ISO-10303-21;
HEADER;
/* Generated by software containing ST-Developer
 * from STEP Tools, Inc. (www.steptools.com) 
 */

FILE_DESCRIPTION(
/* description */ ('Bell-crank linkage with push rods'),
/* implementation_level */ '2;1');

FILE_NAME(
/* name */ 'M5x14 Cap Screw.step',
/* time_stamp */ '2026-10-28T03:25:15-07:00',
/* author */ (''),
/* organization */ (''),
/* preprocessor_version */ 'ST-DEVELOPER v20.2',
/* originating_system */ 'Autodesk Translation Framework v15.17.0.0',
/* authorisation */ '');

FILE_SCHEMA (('AUTOMOTIVE_DESIGN { 1 0 10303 214 3 1 1 }'));
ENDSEC;

DATA;
#10=MECHANICAL_DESIGN_GEOMETRIC_PRESENTATION_REPRESENTATION('',(#613),#16678);
#433=CONICAL_SURFACE('',#9777,0.4,0.785398163397448);
#434=CONICAL_SURFACE('',#9781,0.41,0.785398163397448);
#435=CONICAL_SURFACE('',#9785,0.26,0.463647609000806);
#451=ORIENTED_CLOSED_SHELL('',*,#8803,.F.);
#454=BREP_WITH_VOIDS('Body1',#8804,(#451));
#505=SHAPE_REPRESENTATION_RELATIONSHIP('SRR','None',#16921,#559);
#559=ADVANCED_BREP_SHAPE_REPRESENTATION('',(#454),#16626);
#613=STYLED_ITEM('',(#17298),#454);
#812=FACE_BOUND('',#2017,.T.);
#1043=PLANE('',#9765);
#1044=PLANE('',#9766);
#1045=PLANE('',#9767);
#1046=PLANE('',#9768);
#1047=PLANE('',#9769);
#1048=PLANE('',#9770);
#1049=PLANE('',#9771);
#1050=PLANE('',#9772);
#1051=PLANE('',#9773);
#1052=PLANE('',#9775);
#1053=PLANE('',#9783);
#1394=FACE_OUTER_BOUND('',#2003,.T.);
#1395=FACE_OUTER_BOUND('',#2004,.T.);
#1396=FACE_OUTER_BOUND('',#2005,.T.);
#1397=FACE_OUTER_BOUND('',#2006,.T.);
#1398=FACE_OUTER_BOUND('',#2007,.T.);
#1399=FACE_OUTER_BOUND('',#2008,.T.);
#1400=FACE_OUTER_BOUND('',#2009,.T.);
#1401=FACE_OUTER_BOUND('',#2010,.T.);
#1402=FACE_OUTER_BOUND('',#2011,.T.);
#1403=FACE_OUTER_BOUND('',#2012,.T.);
#1404=FACE_OUTER_BOUND('',#2013,.T.);
#1405=FACE_OUTER_BOUND('',#2014,.T.);
#1406=FACE_OUTER_BOUND('',#2015,.T.);
#1407=FACE_OUTER_BOUND('',#2016,.T.);
#1408=FACE_OUTER_BOUND('',#2018,.T.);
#1409=FACE_OUTER_BOUND('',#2019,.T.);
#2003=EDGE_LOOP('',(#6615,#6616,#6617,#6618));
#2004=EDGE_LOOP('',(#6619,#6620,#6621,#6622));
#2005=EDGE_LOOP('',(#6623,#6624,#6625,#6626));
#2006=EDGE_LOOP('',(#6627,#6628,#6629,#6630));
#2007=EDGE_LOOP('',(#6631,#6632,#6633,#6634));
#2008=EDGE_LOOP('',(#6635,#6636,#6637,#6638));
#2009=EDGE_LOOP('',(#6639,#6640,#6641,#6642,#6643,#6644));
#2010=EDGE_LOOP('',(#6645,#6646,#6647,#6648,#6649,#6650));
#2011=EDGE_LOOP('',(#6651));
#2012=EDGE_LOOP('',(#6652));
#2013=EDGE_LOOP('',(#6653,#6654,#6655,#6656));
#2014=EDGE_LOOP('',(#6657,#6658,#6659,#6660));
#2015=EDGE_LOOP('',(#6661,#6662,#6663,#6664));
#2016=EDGE_LOOP('',(#6665));
#2017=EDGE_LOOP('',(#6666));
#2018=EDGE_LOOP('',(#6667,#6668,#6669,#6670));
#2019=EDGE_LOOP('',(#6671,#6672,#6673,#6674));
#2716=LINE('',#14413,#3265);
#2717=LINE('',#14415,#3266);
#2718=LINE('',#14417,#3267);
#2719=LINE('',#14418,#3268);
#2720=LINE('',#14421,#3269);
#2721=LINE('',#14423,#3270);
#2722=LINE('',#14424,#3271);
#2723=LINE('',#14427,#3272);
#2724=LINE('',#14429,#3273);
#2725=LINE('',#14430,#3274);
#2726=LINE('',#14433,#3275);
#2727=LINE('',#14435,#3276);
#2728=LINE('',#14436,#3277);
#2729=LINE('',#14439,#3278);
#2730=LINE('',#14441,#3279);
#2731=LINE('',#14442,#3280);
#2732=LINE('',#14444,#3281);
#2733=LINE('',#14445,#3282);
#2734=LINE('',#14457,#3283);
#2735=LINE('',#14461,#3284);
#2736=LINE('',#14465,#3285);
#2737=LINE('',#14472,#3286);
#2738=LINE('',#14474,#3287);
#3265=VECTOR('',#11438,1.);
#3266=VECTOR('',#11439,1.);
#3267=VECTOR('',#11440,1.);
#3268=VECTOR('',#11441,1.);
#3269=VECTOR('',#11444,1.);
#3270=VECTOR('',#11445,1.);
#3271=VECTOR('',#11446,1.);
#3272=VECTOR('',#11449,1.);
#3273=VECTOR('',#11450,1.);
#3274=VECTOR('',#11451,1.);
#3275=VECTOR('',#11454,1.);
#3276=VECTOR('',#11455,1.);
#3277=VECTOR('',#11456,1.);
#3278=VECTOR('',#11459,1.);
#3279=VECTOR('',#11460,1.);
#3280=VECTOR('',#11461,1.);
#3281=VECTOR('',#11464,1.);
#3282=VECTOR('',#11465,1.);
#3283=VECTOR('',#11482,0.4);
#3284=VECTOR('',#11487,0.425);
#3285=VECTOR('',#11492,0.41);
#3286=VECTOR('',#11501,0.26);
#3287=VECTOR('',#11504,0.25);
#3782=CIRCLE('',#9774,0.24505);
#3783=CIRCLE('',#9776,0.375);
#3784=CIRCLE('',#9778,0.425);
#3785=CIRCLE('',#9780,0.425);
#3786=CIRCLE('',#9782,0.395);
#3787=CIRCLE('',#9784,0.27);
#3788=CIRCLE('',#9786,0.24505);
#4344=VERTEX_POINT('',#14411);
#4345=VERTEX_POINT('',#14412);
#4346=VERTEX_POINT('',#14414);
#4347=VERTEX_POINT('',#14416);
#4348=VERTEX_POINT('',#14420);
#4349=VERTEX_POINT('',#14422);
#4350=VERTEX_POINT('',#14426);
#4351=VERTEX_POINT('',#14428);
#4352=VERTEX_POINT('',#14432);
#4353=VERTEX_POINT('',#14434);
#4354=VERTEX_POINT('',#14438);
#4355=VERTEX_POINT('',#14440);
#4356=VERTEX_POINT('',#14449);
#4357=VERTEX_POINT('',#14452);
#4358=VERTEX_POINT('',#14455);
#4359=VERTEX_POINT('',#14459);
#4360=VERTEX_POINT('',#14463);
#4361=VERTEX_POINT('',#14467);
#4362=VERTEX_POINT('',#14470);
#5185=EDGE_CURVE('',#4344,#4345,#2716,.T.);
#5186=EDGE_CURVE('',#4345,#4346,#2717,.T.);
#5187=EDGE_CURVE('',#4346,#4347,#2718,.T.);
#5188=EDGE_CURVE('',#4344,#4347,#2719,.T.);
#5189=EDGE_CURVE('',#4345,#4348,#2720,.T.);
#5190=EDGE_CURVE('',#4348,#4349,#2721,.T.);
#5191=EDGE_CURVE('',#4349,#4346,#2722,.T.);
#5192=EDGE_CURVE('',#4348,#4350,#2723,.T.);
#5193=EDGE_CURVE('',#4350,#4351,#2724,.T.);
#5194=EDGE_CURVE('',#4351,#4349,#2725,.T.);
#5195=EDGE_CURVE('',#4350,#4352,#2726,.T.);
#5196=EDGE_CURVE('',#4352,#4353,#2727,.T.);
#5197=EDGE_CURVE('',#4353,#4351,#2728,.T.);
#5198=EDGE_CURVE('',#4352,#4354,#2729,.T.);
#5199=EDGE_CURVE('',#4354,#4355,#2730,.T.);
#5200=EDGE_CURVE('',#4355,#4353,#2731,.T.);
#5201=EDGE_CURVE('',#4354,#4344,#2732,.T.);
#5202=EDGE_CURVE('',#4347,#4355,#2733,.T.);
#5203=EDGE_CURVE('',#4356,#4356,#3782,.T.);
#5204=EDGE_CURVE('',#4357,#4357,#3783,.T.);
#5205=EDGE_CURVE('',#4358,#4358,#3784,.T.);
#5206=EDGE_CURVE('',#4358,#4357,#2734,.T.);
#5207=EDGE_CURVE('',#4359,#4359,#3785,.T.);
#5208=EDGE_CURVE('',#4359,#4358,#2735,.T.);
#5209=EDGE_CURVE('',#4360,#4360,#3786,.T.);
#5210=EDGE_CURVE('',#4360,#4359,#2736,.T.);
#5211=EDGE_CURVE('',#4361,#4361,#3787,.T.);
#5212=EDGE_CURVE('',#4362,#4362,#3788,.F.);
#5213=EDGE_CURVE('',#4362,#4361,#2737,.T.);
#5214=EDGE_CURVE('',#4356,#4362,#2738,.T.);
#6615=ORIENTED_EDGE('',*,*,#5185,.T.);
#6616=ORIENTED_EDGE('',*,*,#5186,.T.);
#6617=ORIENTED_EDGE('',*,*,#5187,.T.);
#6618=ORIENTED_EDGE('',*,*,#5188,.F.);
#6619=ORIENTED_EDGE('',*,*,#5189,.T.);
#6620=ORIENTED_EDGE('',*,*,#5190,.T.);
#6621=ORIENTED_EDGE('',*,*,#5191,.T.);
#6622=ORIENTED_EDGE('',*,*,#5186,.F.);
#6623=ORIENTED_EDGE('',*,*,#5192,.T.);
#6624=ORIENTED_EDGE('',*,*,#5193,.T.);
#6625=ORIENTED_EDGE('',*,*,#5194,.T.);
#6626=ORIENTED_EDGE('',*,*,#5190,.F.);
#6627=ORIENTED_EDGE('',*,*,#5195,.T.);
#6628=ORIENTED_EDGE('',*,*,#5196,.T.);
#6629=ORIENTED_EDGE('',*,*,#5197,.T.);
#6630=ORIENTED_EDGE('',*,*,#5193,.F.);
#6631=ORIENTED_EDGE('',*,*,#5198,.T.);
#6632=ORIENTED_EDGE('',*,*,#5199,.T.);
#6633=ORIENTED_EDGE('',*,*,#5200,.T.);
#6634=ORIENTED_EDGE('',*,*,#5196,.F.);
#6635=ORIENTED_EDGE('',*,*,#5201,.T.);
#6636=ORIENTED_EDGE('',*,*,#5188,.T.);
#6637=ORIENTED_EDGE('',*,*,#5202,.T.);
#6638=ORIENTED_EDGE('',*,*,#5199,.F.);
#6639=ORIENTED_EDGE('',*,*,#5201,.F.);
#6640=ORIENTED_EDGE('',*,*,#5198,.F.);
#6641=ORIENTED_EDGE('',*,*,#5195,.F.);
#6642=ORIENTED_EDGE('',*,*,#5192,.F.);
#6643=ORIENTED_EDGE('',*,*,#5189,.F.);
#6644=ORIENTED_EDGE('',*,*,#5185,.F.);
#6645=ORIENTED_EDGE('',*,*,#5202,.F.);
#6646=ORIENTED_EDGE('',*,*,#5187,.F.);
#6647=ORIENTED_EDGE('',*,*,#5191,.F.);
#6648=ORIENTED_EDGE('',*,*,#5194,.F.);
#6649=ORIENTED_EDGE('',*,*,#5197,.F.);
#6650=ORIENTED_EDGE('',*,*,#5200,.F.);
#6651=ORIENTED_EDGE('',*,*,#5203,.F.);
#6652=ORIENTED_EDGE('',*,*,#5204,.F.);
#6653=ORIENTED_EDGE('',*,*,#5205,.F.);
#6654=ORIENTED_EDGE('',*,*,#5206,.T.);
#6655=ORIENTED_EDGE('',*,*,#5204,.T.);
#6656=ORIENTED_EDGE('',*,*,#5206,.F.);
#6657=ORIENTED_EDGE('',*,*,#5207,.F.);
#6658=ORIENTED_EDGE('',*,*,#5208,.T.);
#6659=ORIENTED_EDGE('',*,*,#5205,.T.);
#6660=ORIENTED_EDGE('',*,*,#5208,.F.);
#6661=ORIENTED_EDGE('',*,*,#5209,.F.);
#6662=ORIENTED_EDGE('',*,*,#5210,.T.);
#6663=ORIENTED_EDGE('',*,*,#5207,.T.);
#6664=ORIENTED_EDGE('',*,*,#5210,.F.);
#6665=ORIENTED_EDGE('',*,*,#5209,.T.);
#6666=ORIENTED_EDGE('',*,*,#5211,.F.);
#6667=ORIENTED_EDGE('',*,*,#5212,.F.);
#6668=ORIENTED_EDGE('',*,*,#5213,.T.);
#6669=ORIENTED_EDGE('',*,*,#5211,.T.);
#6670=ORIENTED_EDGE('',*,*,#5213,.F.);
#6671=ORIENTED_EDGE('',*,*,#5203,.T.);
#6672=ORIENTED_EDGE('',*,*,#5214,.T.);
#6673=ORIENTED_EDGE('',*,*,#5212,.T.);
#6674=ORIENTED_EDGE('',*,*,#5214,.F.);
#8137=CYLINDRICAL_SURFACE('',#9779,0.425);
#8138=CYLINDRICAL_SURFACE('',#9787,0.24505);
#8419=ADVANCED_FACE('',(#1394),#1043,.F.);
#8420=ADVANCED_FACE('',(#1395),#1044,.F.);
#8421=ADVANCED_FACE('',(#1396),#1045,.F.);
#8422=ADVANCED_FACE('',(#1397),#1046,.F.);
#8423=ADVANCED_FACE('',(#1398),#1047,.F.);
#8424=ADVANCED_FACE('',(#1399),#1048,.F.);
#8425=ADVANCED_FACE('',(#1400),#1049,.F.);
#8426=ADVANCED_FACE('',(#1401),#1050,.F.);
#8427=ADVANCED_FACE('',(#1402),#1051,.F.);
#8428=ADVANCED_FACE('',(#1403),#1052,.T.);
#8429=ADVANCED_FACE('',(#1404),#433,.T.);
#8430=ADVANCED_FACE('',(#1405),#8137,.T.);
#8431=ADVANCED_FACE('',(#1406),#434,.T.);
#8432=ADVANCED_FACE('',(#1407,#812),#1053,.T.);
#8433=ADVANCED_FACE('',(#1408),#435,.T.);
#8434=ADVANCED_FACE('',(#1409),#8138,.T.);
#8803=CLOSED_SHELL('',(#8419,#8420,#8421,#8422,#8423,#8424,#8425,#8426));
#8804=CLOSED_SHELL('',(#8427,#8428,#8429,#8430,#8431,#8432,#8433,#8434));
#9764=AXIS2_PLACEMENT_3D('',#14409,#11434,#11435);
#9765=AXIS2_PLACEMENT_3D('',#14410,#11436,#11437);
#9766=AXIS2_PLACEMENT_3D('',#14419,#11442,#11443);
#9767=AXIS2_PLACEMENT_3D('',#14425,#11447,#11448);
#9768=AXIS2_PLACEMENT_3D('',#14431,#11452,#11453);
#9769=AXIS2_PLACEMENT_3D('',#14437,#11457,#11458);
#9770=AXIS2_PLACEMENT_3D('',#14443,#11462,#11463);
#9771=AXIS2_PLACEMENT_3D('',#14446,#11466,#11467);
#9772=AXIS2_PLACEMENT_3D('',#14447,#11468,#11469);
#9773=AXIS2_PLACEMENT_3D('',#14448,#11470,#11471);
#9774=AXIS2_PLACEMENT_3D('',#14450,#11472,#11473);
#9775=AXIS2_PLACEMENT_3D('',#14451,#11474,#11475);
#9776=AXIS2_PLACEMENT_3D('',#14453,#11476,#11477);
#9777=AXIS2_PLACEMENT_3D('',#14454,#11478,#11479);
#9778=AXIS2_PLACEMENT_3D('',#14456,#11480,#11481);
#9779=AXIS2_PLACEMENT_3D('',#14458,#11483,#11484);
#9780=AXIS2_PLACEMENT_3D('',#14460,#11485,#11486);
#9781=AXIS2_PLACEMENT_3D('',#14462,#11488,#11489);
#9782=AXIS2_PLACEMENT_3D('',#14464,#11490,#11491);
#9783=AXIS2_PLACEMENT_3D('',#14466,#11493,#11494);
#9784=AXIS2_PLACEMENT_3D('',#14468,#11495,#11496);
#9785=AXIS2_PLACEMENT_3D('',#14469,#11497,#11498);
#9786=AXIS2_PLACEMENT_3D('',#14471,#11499,#11500);
#9787=AXIS2_PLACEMENT_3D('',#14473,#11502,#11503);
#11434=DIRECTION('axis',(0.,0.,1.));
#11435=DIRECTION('refdir',(1.,0.,0.));
#11436=DIRECTION('center_axis',(0.866025403784439,0.,-0.5));
#11437=DIRECTION('ref_axis',(0.5,0.,0.866025403784439));
#11438=DIRECTION('',(-0.5,0.,-0.866025403784439));
#11439=DIRECTION('',(0.,-1.,0.));
#11440=DIRECTION('',(0.5,0.,0.866025403784439));
#11441=DIRECTION('',(0.,-1.,0.));
#11442=DIRECTION('center_axis',(1.20185167898973E-16,0.,-1.));
#11443=DIRECTION('ref_axis',(1.,0.,1.20185167898973E-16));
#11444=DIRECTION('',(-1.,0.,-1.20185167898973E-16));
#11445=DIRECTION('',(0.,-1.,0.));
#11446=DIRECTION('',(1.,0.,1.20185167898973E-16));
#11447=DIRECTION('center_axis',(-0.866025403784439,0.,-0.5));
#11448=DIRECTION('ref_axis',(0.5,0.,-0.866025403784439));
#11449=DIRECTION('',(-0.5,0.,0.866025403784439));
#11450=DIRECTION('',(0.,-1.,0.));
#11451=DIRECTION('',(0.5,0.,-0.866025403784439));
#11452=DIRECTION('center_axis',(-0.866025403784439,0.,0.5));
#11453=DIRECTION('ref_axis',(-0.5,0.,-0.866025403784439));
#11454=DIRECTION('',(0.5,0.,0.866025403784439));
#11455=DIRECTION('',(0.,-1.,0.));
#11456=DIRECTION('',(-0.5,0.,-0.866025403784439));
#11457=DIRECTION('center_axis',(-2.40370335797945E-16,0.,1.));
#11458=DIRECTION('ref_axis',(-1.,0.,-2.40370335797945E-16));
#11459=DIRECTION('',(1.,0.,2.40370335797945E-16));
#11460=DIRECTION('',(0.,-1.,0.));
#11461=DIRECTION('',(-1.,0.,-2.40370335797945E-16));
#11462=DIRECTION('center_axis',(0.866025403784439,0.,0.5));
#11463=DIRECTION('ref_axis',(-0.5,0.,0.866025403784439));
#11464=DIRECTION('',(0.5,0.,-0.866025403784439));
#11465=DIRECTION('',(-0.5,0.,0.866025403784439));
#11466=DIRECTION('center_axis',(0.,1.,0.));
#11467=DIRECTION('ref_axis',(1.,0.,0.));
#11468=DIRECTION('center_axis',(0.,-1.,0.));
#11469=DIRECTION('ref_axis',(0.,0.,-1.));
#11470=DIRECTION('center_axis',(0.,1.,0.));
#11471=DIRECTION('ref_axis',(1.,0.,0.));
#11472=DIRECTION('center_axis',(0.,1.,0.));
#11473=DIRECTION('ref_axis',(1.,0.,0.));
#11474=DIRECTION('center_axis',(0.,1.,0.));
#11475=DIRECTION('ref_axis',(0.,0.,1.));
#11476=DIRECTION('center_axis',(0.,-1.,0.));
#11477=DIRECTION('ref_axis',(1.,0.,0.));
#11478=DIRECTION('center_axis',(0.,-1.,0.));
#11479=DIRECTION('ref_axis',(1.,0.,0.));
#11480=DIRECTION('center_axis',(0.,-1.,0.));
#11481=DIRECTION('ref_axis',(1.,0.,0.));
#11482=DIRECTION('',(0.707106781186548,0.707106781186547,8.65956056235493E-17));
#11483=DIRECTION('center_axis',(0.,-1.,0.));
#11484=DIRECTION('ref_axis',(1.,0.,0.));
#11485=DIRECTION('center_axis',(0.,-1.,0.));
#11486=DIRECTION('ref_axis',(1.,0.,0.));
#11487=DIRECTION('',(0.,1.,0.));
#11488=DIRECTION('center_axis',(0.,1.,0.));
#11489=DIRECTION('ref_axis',(1.,0.,0.));
#11490=DIRECTION('center_axis',(0.,-1.,0.));
#11491=DIRECTION('ref_axis',(1.,0.,0.));
#11492=DIRECTION('',(-0.707106781186547,0.707106781186548,-8.65956056235493E-17));
#11493=DIRECTION('center_axis',(0.,-1.,0.));
#11494=DIRECTION('ref_axis',(0.,0.,-1.));
#11495=DIRECTION('center_axis',(0.,-1.,0.));
#11496=DIRECTION('ref_axis',(1.,0.,0.));
#11497=DIRECTION('center_axis',(0.,1.,0.));
#11498=DIRECTION('ref_axis',(1.,0.,0.));
#11499=DIRECTION('center_axis',(0.,1.,0.));
#11500=DIRECTION('ref_axis',(1.,0.,0.));
#11501=DIRECTION('',(-0.447213595499958,0.894427190999916,-5.47678698264203E-17));
#11502=DIRECTION('center_axis',(0.,-1.,0.));
#11503=DIRECTION('ref_axis',(1.,0.,0.));
#11504=DIRECTION('',(0.,1.,0.));
#14409=CARTESIAN_POINT('',(0.,0.,0.));
#14410=CARTESIAN_POINT('Origin',(0.115470053837925,-0.5,-0.2));
#14411=CARTESIAN_POINT('',(0.23094010767585,-0.5,0.));
#14412=CARTESIAN_POINT('',(0.115470053837925,-0.5,-0.2));
#14413=CARTESIAN_POINT('',(0.23094010767585,-0.5,0.));
#14414=CARTESIAN_POINT('',(0.115470053837925,-0.8,-0.2));
#14415=CARTESIAN_POINT('',(0.115470053837925,-0.5,-0.2));
#14416=CARTESIAN_POINT('',(0.23094010767585,-0.8,0.));
#14417=CARTESIAN_POINT('',(0.23094010767585,-0.8,0.));
#14418=CARTESIAN_POINT('',(0.23094010767585,-0.5,0.));
#14419=CARTESIAN_POINT('Origin',(-0.115470053837925,-0.5,-0.2));
#14420=CARTESIAN_POINT('',(-0.115470053837925,-0.5,-0.2));
#14421=CARTESIAN_POINT('',(0.115470053837925,-0.5,-0.2));
#14422=CARTESIAN_POINT('',(-0.115470053837925,-0.8,-0.2));
#14423=CARTESIAN_POINT('',(-0.115470053837925,-0.5,-0.2));
#14424=CARTESIAN_POINT('',(0.115470053837925,-0.8,-0.2));
#14425=CARTESIAN_POINT('Origin',(-0.23094010767585,-0.5,-2.77555756156289E-17));
#14426=CARTESIAN_POINT('',(-0.23094010767585,-0.5,-2.82820063659975E-17));
#14427=CARTESIAN_POINT('',(-0.115470053837925,-0.5,-0.2));
#14428=CARTESIAN_POINT('',(-0.23094010767585,-0.8,-2.77555756156289E-17));
#14429=CARTESIAN_POINT('',(-0.23094010767585,-0.5,-2.82820063659975E-17));
#14430=CARTESIAN_POINT('',(-0.115470053837925,-0.8,-0.2));
#14431=CARTESIAN_POINT('Origin',(-0.115470053837925,-0.5,0.2));
#14432=CARTESIAN_POINT('',(-0.115470053837925,-0.5,0.2));
#14433=CARTESIAN_POINT('',(-0.23094010767585,-0.5,-2.82820063659975E-17));
#14434=CARTESIAN_POINT('',(-0.115470053837925,-0.8,0.2));
#14435=CARTESIAN_POINT('',(-0.115470053837925,-0.5,0.2));
#14436=CARTESIAN_POINT('',(-0.23094010767585,-0.8,-2.82820063659975E-17));
#14437=CARTESIAN_POINT('Origin',(0.115470053837925,-0.5,0.2));
#14438=CARTESIAN_POINT('',(0.115470053837925,-0.5,0.2));
#14439=CARTESIAN_POINT('',(-0.115470053837925,-0.5,0.2));
#14440=CARTESIAN_POINT('',(0.115470053837925,-0.8,0.2));
#14441=CARTESIAN_POINT('',(0.115470053837925,-0.5,0.2));
#14442=CARTESIAN_POINT('',(-0.115470053837925,-0.8,0.2));
#14443=CARTESIAN_POINT('Origin',(0.23094010767585,-0.5,0.));
#14444=CARTESIAN_POINT('',(0.115470053837925,-0.5,0.2));
#14445=CARTESIAN_POINT('',(0.115470053837925,-0.8,0.2));
#14446=CARTESIAN_POINT('Origin',(0.,-0.5,0.));
#14447=CARTESIAN_POINT('Origin',(0.,-0.8,0.));
#14448=CARTESIAN_POINT('Origin',(0.,-1.4,0.));
#14449=CARTESIAN_POINT('',(-0.24505,-1.4,3.00099698131059E-17));
#14450=CARTESIAN_POINT('Origin',(0.,-1.4,0.));
#14451=CARTESIAN_POINT('Origin',(0.375,0.5,0.));
#14452=CARTESIAN_POINT('',(-0.375,0.5,-4.59242549680257E-17));
#14453=CARTESIAN_POINT('Origin',(0.,0.5,0.));
#14454=CARTESIAN_POINT('Origin',(0.,0.475,0.));
#14455=CARTESIAN_POINT('',(-0.425,0.45,-5.20474889637625E-17));
#14456=CARTESIAN_POINT('Origin',(0.,0.45,0.));
#14457=CARTESIAN_POINT('',(-0.4,0.475,-4.89858719658941E-17));
#14458=CARTESIAN_POINT('Origin',(0.,0.24,0.));
#14459=CARTESIAN_POINT('',(-0.425,0.0299999999999998,-5.20474889637625E-17));
#14460=CARTESIAN_POINT('Origin',(0.,0.0299999999999998,0.));
#14461=CARTESIAN_POINT('',(-0.425,0.24,-5.20474889637625E-17));
#14462=CARTESIAN_POINT('Origin',(0.,0.0150000000000001,0.));
#14463=CARTESIAN_POINT('',(-0.395,4.85722573273506E-17,-4.83735485663204E-17));
#14464=CARTESIAN_POINT('Origin',(0.,0.,0.));
#14465=CARTESIAN_POINT('',(-0.41,0.0150000000000001,-5.02105187650415E-17));
#14466=CARTESIAN_POINT('Origin',(0.27,0.,0.));
#14467=CARTESIAN_POINT('',(-0.27,0.,-3.30654635769785E-17));
#14468=CARTESIAN_POINT('Origin',(0.,0.,0.));
#14469=CARTESIAN_POINT('Origin',(0.,-0.02,0.));
#14470=CARTESIAN_POINT('',(-0.24505,-0.0498999999999999,3.00099698131059E-17));
#14471=CARTESIAN_POINT('Origin',(0.,-0.0498999999999999,0.));
#14472=CARTESIAN_POINT('',(-0.26,-0.02,-3.18408167778312E-17));
#14473=CARTESIAN_POINT('Origin',(0.,-0.995,0.));
#14474=CARTESIAN_POINT('',(-0.24505,-0.995,-3.00099698131059E-17));
#16562=UNCERTAINTY_MEASURE_WITH_UNIT(LENGTH_MEASURE(0.001),#16679,
'DISTANCE_ACCURACY_VALUE',
'Maximum model space distance between geometric entities at asserted c
onnectivities');
#16614=UNCERTAINTY_MEASURE_WITH_UNIT(LENGTH_MEASURE(0.001),#16679,
'DISTANCE_ACCURACY_VALUE',
'Maximum model space distance between geometric entities at asserted c
onnectivities');
#16626=(
GEOMETRIC_REPRESENTATION_CONTEXT(3)
GLOBAL_UNCERTAINTY_ASSIGNED_CONTEXT((#16562))
GLOBAL_UNIT_ASSIGNED_CONTEXT((#16679,#16681,#16682))
REPRESENTATION_CONTEXT('','3D')
);
#16678=(
GEOMETRIC_REPRESENTATION_CONTEXT(3)
GLOBAL_UNCERTAINTY_ASSIGNED_CONTEXT((#16614))
GLOBAL_UNIT_ASSIGNED_CONTEXT((#16679,#16681,#16682))
REPRESENTATION_CONTEXT('','3D')
);
#16679=(
LENGTH_UNIT()
NAMED_UNIT(*)
SI_UNIT(.CENTI.,.METRE.)
);
#16681=(
NAMED_UNIT(*)
PLANE_ANGLE_UNIT()
SI_UNIT($,.RADIAN.)
);
#16682=(
NAMED_UNIT(*)
SI_UNIT($,.STERADIAN.)
SOLID_ANGLE_UNIT()
);
#16694=SHAPE_DEFINITION_REPRESENTATION(#16757,#16921);
#16757=PRODUCT_DEFINITION_SHAPE('',$,#16985);
#16921=SHAPE_REPRESENTATION('',(#9764),#16626);
#16973=PRODUCT_DEFINITION_CONTEXT('part definition',#17164,'design');
#16985=PRODUCT_DEFINITION('M5x14 Cap Screw','M5x14 Cap Screw',#17048,#16973);
#17048=PRODUCT_DEFINITION_FORMATION('',$,#17177);
#17164=APPLICATION_CONTEXT(
'Core Data for Automotive Mechanical Design Process');
#17165=PRODUCT_CONTEXT('part definition',#17164,'mechanical');
#17177=PRODUCT('M5x14 Cap Screw','M5x14 Cap Screw','M5x14 Cap Screw',(#17165));
#17292=COLOUR_RGB('Black',0.12,0.14,0.17);
#17293=FILL_AREA_STYLE_COLOUR('',#17292);
#17294=FILL_AREA_STYLE('',(#17293));
#17295=SURFACE_STYLE_FILL_AREA(#17294);
#17296=SURFACE_SIDE_STYLE('',(#17295));
#17297=SURFACE_STYLE_USAGE(.BOTH.,#17296);
#17298=PRESENTATION_STYLE_ASSIGNMENT((#17297));
ENDSEC;
END-ISO-10303-21;
